ISO-10303-21;
HEADER;
/* Generated by software containing ST-Developer
 * from STEP Tools, Inc. (www.steptools.com) 
 */

FILE_DESCRIPTION(
/* description */ (''),
/* implementation_level */ '2;1');

FILE_NAME(
/* name */ 'Feed Screw End Block.step',
/* time_stamp */ '2026-10-15T12:29:06-07:00',
/* author */ (''),
/* organization */ (''),
/* preprocessor_version */ 'ST-DEVELOPER v20.2',
/* originating_system */ 'Autodesk Translation Framework v15.15.0.0',
/* authorisation */ '');

FILE_SCHEMA (('AUTOMOTIVE_DESIGN { 1 0 10303 214 3 1 1 }'));
ENDSEC;

DATA;
#10=MECHANICAL_DESIGN_GEOMETRIC_PRESENTATION_REPRESENTATION('',(#1748),#135282);
#1722=SHAPE_REPRESENTATION_RELATIONSHIP('SRR','None',#135346,#1735);
#1735=ADVANCED_BREP_SHAPE_REPRESENTATION('',(#1761),#135278);
#1748=STYLED_ITEM('',(#135420),#1761);
#1761=MANIFOLD_SOLID_BREP('Body1',#32084);
#1881=CYLINDRICAL_SURFACE('',#33497,1.05);
#1882=CYLINDRICAL_SURFACE('',#33505,1.05);
#1883=CYLINDRICAL_SURFACE('',#33518,1.55);
#1884=CYLINDRICAL_SURFACE('',#33522,1.55);
#1885=CYLINDRICAL_SURFACE('',#33528,3.);
#1886=CYLINDRICAL_SURFACE('',#33532,3.);
#1887=CYLINDRICAL_SURFACE('',#33538,1.7);
#1888=CYLINDRICAL_SURFACE('',#33540,1.7);
#1889=CYLINDRICAL_SURFACE('',#33545,2.015);
#2215=FACE_BOUND('',#6605,.T.);
#2216=FACE_BOUND('',#6610,.T.);
#2217=FACE_BOUND('',#6614,.T.);
#2218=FACE_BOUND('',#6615,.T.);
#2219=FACE_BOUND('',#6616,.T.);
#2220=FACE_BOUND('',#6617,.T.);
#2221=FACE_BOUND('',#6618,.T.);
#2222=FACE_BOUND('',#6629,.T.);
#2223=FACE_BOUND('',#6631,.T.);
#2224=FACE_BOUND('',#6637,.T.);
#2225=FACE_BOUND('',#6638,.T.);
#2226=FACE_BOUND('',#6639,.T.);
#3064=PLANE('',#33500);
#3065=PLANE('',#33508);
#3066=PLANE('',#33513);
#3067=PLANE('',#33534);
#3068=PLANE('',#33536);
#3069=PLANE('',#33547);
#3070=PLANE('',#33549);
#3071=PLANE('',#33550);
#3072=PLANE('',#33551);
#3073=PLANE('',#33552);
#3074=PLANE('',#33553);
#3075=PLANE('',#33554);
#4649=FACE_OUTER_BOUND('',#6602,.T.);
#4650=FACE_OUTER_BOUND('',#6603,.T.);
#4651=FACE_OUTER_BOUND('',#6604,.T.);
#4652=FACE_OUTER_BOUND('',#6606,.T.);
#4653=FACE_OUTER_BOUND('',#6607,.T.);
#4654=FACE_OUTER_BOUND('',#6608,.T.);
#4655=FACE_OUTER_BOUND('',#6609,.T.);
#4656=FACE_OUTER_BOUND('',#6611,.T.);
#4657=FACE_OUTER_BOUND('',#6612,.T.);
#4658=FACE_OUTER_BOUND('',#6613,.T.);
#4659=FACE_OUTER_BOUND('',#6619,.T.);
#4660=FACE_OUTER_BOUND('',#6620,.T.);
#4661=FACE_OUTER_BOUND('',#6621,.T.);
#4662=FACE_OUTER_BOUND('',#6622,.T.);
#4663=FACE_OUTER_BOUND('',#6623,.T.);
#4664=FACE_OUTER_BOUND('',#6624,.T.);
#4665=FACE_OUTER_BOUND('',#6625,.T.);
#4666=FACE_OUTER_BOUND('',#6626,.T.);
#4667=FACE_OUTER_BOUND('',#6627,.T.);
#4668=FACE_OUTER_BOUND('',#6628,.T.);
#4669=FACE_OUTER_BOUND('',#6630,.T.);
#4670=FACE_OUTER_BOUND('',#6632,.T.);
#4671=FACE_OUTER_BOUND('',#6633,.T.);
#4672=FACE_OUTER_BOUND('',#6634,.T.);
#4673=FACE_OUTER_BOUND('',#6635,.T.);
#4674=FACE_OUTER_BOUND('',#6636,.T.);
#4675=FACE_OUTER_BOUND('',#6640,.T.);
#4676=FACE_OUTER_BOUND('',#6641,.T.);
#4677=FACE_OUTER_BOUND('',#6642,.T.);
#4678=FACE_OUTER_BOUND('',#6643,.T.);
#4679=FACE_OUTER_BOUND('',#6644,.T.);
#4680=FACE_OUTER_BOUND('',#6645,.T.);
#4681=FACE_OUTER_BOUND('',#6646,.T.);
#6602=EDGE_LOOP('',(#27636,#27637,#27638,#27639));
#6603=EDGE_LOOP('',(#27640,#27641,#27642,#27643,#27644));
#6604=EDGE_LOOP('',(#27645,#27646,#27647,#27648));
#6605=EDGE_LOOP('',(#27649));
#6606=EDGE_LOOP('',(#27650,#27651,#27652,#27653));
#6607=EDGE_LOOP('',(#27654,#27655,#27656,#27657));
#6608=EDGE_LOOP('',(#27658,#27659,#27660,#27661,#27662));
#6609=EDGE_LOOP('',(#27663,#27664,#27665,#27666));
#6610=EDGE_LOOP('',(#27667));
#6611=EDGE_LOOP('',(#27668,#27669,#27670,#27671));
#6612=EDGE_LOOP('',(#27672,#27673,#27674,#27675));
#6613=EDGE_LOOP('',(#27676,#27677,#27678,#27679,#27680,#27681,#27682,#27683));
#6614=EDGE_LOOP('',(#27684));
#6615=EDGE_LOOP('',(#27685));
#6616=EDGE_LOOP('',(#27686));
#6617=EDGE_LOOP('',(#27687));
#6618=EDGE_LOOP('',(#27688));
#6619=EDGE_LOOP('',(#27689,#27690,#27691,#27692));
#6620=EDGE_LOOP('',(#27693,#27694,#27695,#27696));
#6621=EDGE_LOOP('',(#27697,#27698,#27699,#27700));
#6622=EDGE_LOOP('',(#27701,#27702,#27703));
#6623=EDGE_LOOP('',(#27704,#27705,#27706));
#6624=EDGE_LOOP('',(#27707,#27708,#27709,#27710));
#6625=EDGE_LOOP('',(#27711,#27712,#27713,#27714));
#6626=EDGE_LOOP('',(#27715,#27716,#27717,#27718));
#6627=EDGE_LOOP('',(#27719,#27720,#27721,#27722));
#6628=EDGE_LOOP('',(#27723));
#6629=EDGE_LOOP('',(#27724));
#6630=EDGE_LOOP('',(#27725));
#6631=EDGE_LOOP('',(#27726));
#6632=EDGE_LOOP('',(#27727,#27728,#27729,#27730));
#6633=EDGE_LOOP('',(#27731,#27732,#27733,#27734));
#6634=EDGE_LOOP('',(#27735,#27736,#27737,#27738));
#6635=EDGE_LOOP('',(#27739,#27740,#27741,#27742));
#6636=EDGE_LOOP('',(#27743,#27744,#27745,#27746,#27747,#27748,#27749,#27750));
#6637=EDGE_LOOP('',(#27751));
#6638=EDGE_LOOP('',(#27752));
#6639=EDGE_LOOP('',(#27753));
#6640=EDGE_LOOP('',(#27754,#27755,#27756,#27757));
#6641=EDGE_LOOP('',(#27758,#27759,#27760,#27761));
#6642=EDGE_LOOP('',(#27762,#27763,#27764,#27765));
#6643=EDGE_LOOP('',(#27766,#27767,#27768,#27769));
#6644=EDGE_LOOP('',(#27770,#27771,#27772,#27773));
#6645=EDGE_LOOP('',(#27774,#27775,#27776,#27777));
#6646=EDGE_LOOP('',(#27778,#27779,#27780,#27781));
#9317=LINE('',#84184,#12154);
#9318=LINE('',#84188,#12155);
#9319=LINE('',#84195,#12156);
#9320=LINE('',#84197,#12157);
#9321=LINE('',#84199,#12158);
#9322=LINE('',#84200,#12159);
#9323=LINE('',#84203,#12160);
#9324=LINE('',#84208,#12161);
#9325=LINE('',#84212,#12162);
#9326=LINE('',#84219,#12163);
#9327=LINE('',#84221,#12164);
#9328=LINE('',#84223,#12165);
#9329=LINE('',#84224,#12166);
#9330=LINE('',#84227,#12167);
#9331=LINE('',#84232,#12168);
#9332=LINE('',#84236,#12169);
#9333=LINE('',#84238,#12170);
#9334=LINE('',#84239,#12171);
#9335=LINE('',#84241,#12172);
#9336=LINE('',#84243,#12173);
#9337=LINE('',#84244,#12174);
#9338=LINE('',#84255,#12175);
#9339=LINE('',#84260,#12176);
#9340=LINE('',#84263,#12177);
#9341=LINE('',#84267,#12178);
#9342=LINE('',#84270,#12179);
#9343=LINE('',#84274,#12180);
#9344=LINE('',#84277,#12181);
#9345=LINE('',#84282,#12182);
#9346=LINE('',#84285,#12183);
#9347=LINE('',#84295,#12184);
#9348=LINE('',#84299,#12185);
#9349=LINE('',#84305,#12186);
#9350=LINE('',#84310,#12187);
#9351=LINE('',#84313,#12188);
#9352=LINE('',#84315,#12189);
#9353=LINE('',#84317,#12190);
#9354=LINE('',#84318,#12191);
#9355=LINE('',#84320,#12192);
#9356=LINE('',#84321,#12193);
#9357=LINE('',#84323,#12194);
#9358=LINE('',#84325,#12195);
#9359=LINE('',#84327,#12196);
#9360=LINE('',#84329,#12197);
#9361=LINE('',#84331,#12198);
#12154=VECTOR('',#38999,1.125);
#12155=VECTOR('',#39004,1.05);
#12156=VECTOR('',#39011,10.);
#12157=VECTOR('',#39012,10.);
#12158=VECTOR('',#39013,10.);
#12159=VECTOR('',#39014,10.);
#12160=VECTOR('',#39017,1.05);
#12161=VECTOR('',#39022,1.125);
#12162=VECTOR('',#39027,1.05);
#12163=VECTOR('',#39034,10.);
#12164=VECTOR('',#39035,10.);
#12165=VECTOR('',#39036,10.);
#12166=VECTOR('',#39037,10.);
#12167=VECTOR('',#39040,0.525);
#12168=VECTOR('',#39045,1.65);
#12169=VECTOR('',#39050,9.99999999999999);
#12170=VECTOR('',#39051,10.);
#12171=VECTOR('',#39052,10.);
#12172=VECTOR('',#39053,10.);
#12173=VECTOR('',#39054,10.);
#12174=VECTOR('',#39055,10.);
#12175=VECTOR('',#39066,1.55);
#12176=VECTOR('',#39073,1.65);
#12177=VECTOR('',#39076,1.55);
#12178=VECTOR('',#39081,0.775000000000001);
#12179=VECTOR('',#39084,0.775);
#12180=VECTOR('',#39089,3.15);
#12181=VECTOR('',#39092,3.);
#12182=VECTOR('',#39099,3.15);
#12183=VECTOR('',#39102,3.);
#12184=VECTOR('',#39115,1.7);
#12185=VECTOR('',#39120,1.7);
#12186=VECTOR('',#39127,2.165);
#12187=VECTOR('',#39134,2.015);
#12188=VECTOR('',#39137,9.99999999999999);
#12189=VECTOR('',#39138,10.);
#12190=VECTOR('',#39139,10.);
#12191=VECTOR('',#39140,10.);
#12192=VECTOR('',#39141,10.);
#12193=VECTOR('',#39142,10.);
#12194=VECTOR('',#39145,2.165);
#12195=VECTOR('',#39148,10.);
#12196=VECTOR('',#39151,10.);
#12197=VECTOR('',#39154,10.);
#12198=VECTOR('',#39157,10.);
#12983=CIRCLE('',#33495,1.05);
#12984=CIRCLE('',#33496,1.2);
#12985=CIRCLE('',#33498,1.05);
#12986=CIRCLE('',#33499,1.05);
#12987=CIRCLE('',#33503,1.05);
#12988=CIRCLE('',#33504,1.2);
#12989=CIRCLE('',#33506,1.05);
#12990=CIRCLE('',#33507,1.05);
#12991=CIRCLE('',#33511,1.55);
#12992=CIRCLE('',#33512,1.75);
#12993=CIRCLE('',#33514,1.75);
#12994=CIRCLE('',#33515,3.3);
#12995=CIRCLE('',#33516,2.315);
#12996=CIRCLE('',#33517,3.3);
#12997=CIRCLE('',#33519,1.55);
#12998=CIRCLE('',#33521,1.55);
#12999=CIRCLE('',#33523,1.55);
#13000=CIRCLE('',#33527,3.);
#13001=CIRCLE('',#33529,3.);
#13002=CIRCLE('',#33531,3.);
#13003=CIRCLE('',#33533,3.);
#13004=CIRCLE('',#33535,1.7);
#13005=CIRCLE('',#33537,1.7);
#13006=CIRCLE('',#33539,1.7);
#13007=CIRCLE('',#33541,1.7);
#13008=CIRCLE('',#33543,2.015);
#13009=CIRCLE('',#33544,2.315);
#13010=CIRCLE('',#33546,2.015);
#15464=VERTEX_POINT('',#84181);
#15465=VERTEX_POINT('',#84183);
#15466=VERTEX_POINT('',#84187);
#15467=VERTEX_POINT('',#84189);
#15468=VERTEX_POINT('',#84193);
#15469=VERTEX_POINT('',#84194);
#15470=VERTEX_POINT('',#84196);
#15471=VERTEX_POINT('',#84198);
#15472=VERTEX_POINT('',#84202);
#15473=VERTEX_POINT('',#84205);
#15474=VERTEX_POINT('',#84207);
#15475=VERTEX_POINT('',#84211);
#15476=VERTEX_POINT('',#84213);
#15477=VERTEX_POINT('',#84217);
#15478=VERTEX_POINT('',#84218);
#15479=VERTEX_POINT('',#84220);
#15480=VERTEX_POINT('',#84222);
#15481=VERTEX_POINT('',#84226);
#15482=VERTEX_POINT('',#84229);
#15483=VERTEX_POINT('',#84231);
#15484=VERTEX_POINT('',#84235);
#15485=VERTEX_POINT('',#84237);
#15486=VERTEX_POINT('',#84240);
#15487=VERTEX_POINT('',#84242);
#15488=VERTEX_POINT('',#84245);
#15489=VERTEX_POINT('',#84247);
#15490=VERTEX_POINT('',#84249);
#15491=VERTEX_POINT('',#84251);
#15492=VERTEX_POINT('',#84254);
#15493=VERTEX_POINT('',#84258);
#15494=VERTEX_POINT('',#84262);
#15495=VERTEX_POINT('',#84266);
#15496=VERTEX_POINT('',#84269);
#15497=VERTEX_POINT('',#84272);
#15498=VERTEX_POINT('',#84276);
#15499=VERTEX_POINT('',#84280);
#15500=VERTEX_POINT('',#84284);
#15501=VERTEX_POINT('',#84288);
#15502=VERTEX_POINT('',#84291);
#15503=VERTEX_POINT('',#84294);
#15504=VERTEX_POINT('',#84298);
#15505=VERTEX_POINT('',#84302);
#15506=VERTEX_POINT('',#84304);
#15507=VERTEX_POINT('',#84308);
#15508=VERTEX_POINT('',#84312);
#15509=VERTEX_POINT('',#84314);
#15510=VERTEX_POINT('',#84316);
#15511=VERTEX_POINT('',#84319);
#19669=EDGE_CURVE('',#15464,#15464,#12983,.T.);
#19670=EDGE_CURVE('',#15464,#15465,#9317,.T.);
#19671=EDGE_CURVE('',#15465,#15465,#12984,.T.);
#19672=EDGE_CURVE('',#15464,#15466,#9318,.T.);
#19673=EDGE_CURVE('',#15466,#15467,#12985,.T.);
#19674=EDGE_CURVE('',#15467,#15466,#12986,.T.);
#19675=EDGE_CURVE('',#15468,#15469,#9319,.T.);
#19676=EDGE_CURVE('',#15470,#15468,#9320,.T.);
#19677=EDGE_CURVE('',#15471,#15470,#9321,.T.);
#19678=EDGE_CURVE('',#15469,#15471,#9322,.T.);
#19679=EDGE_CURVE('',#15472,#15467,#9323,.T.);
#19680=EDGE_CURVE('',#15473,#15473,#12987,.T.);
#19681=EDGE_CURVE('',#15473,#15474,#9324,.T.);
#19682=EDGE_CURVE('',#15474,#15474,#12988,.T.);
#19683=EDGE_CURVE('',#15473,#15475,#9325,.T.);
#19684=EDGE_CURVE('',#15475,#15476,#12989,.T.);
#19685=EDGE_CURVE('',#15476,#15475,#12990,.T.);
#19686=EDGE_CURVE('',#15477,#15478,#9326,.T.);
#19687=EDGE_CURVE('',#15479,#15477,#9327,.T.);
#19688=EDGE_CURVE('',#15480,#15479,#9328,.T.);
#19689=EDGE_CURVE('',#15478,#15480,#9329,.T.);
#19690=EDGE_CURVE('',#15481,#15476,#9330,.T.);
#19691=EDGE_CURVE('',#15482,#15482,#12991,.T.);
#19692=EDGE_CURVE('',#15482,#15483,#9331,.T.);
#19693=EDGE_CURVE('',#15483,#15483,#12992,.T.);
#19694=EDGE_CURVE('',#15484,#15477,#9332,.T.);
#19695=EDGE_CURVE('',#15484,#15485,#9333,.T.);
#19696=EDGE_CURVE('',#15470,#15485,#9334,.T.);
#19697=EDGE_CURVE('',#15486,#15468,#9335,.T.);
#19698=EDGE_CURVE('',#15486,#15487,#9336,.T.);
#19699=EDGE_CURVE('',#15479,#15487,#9337,.T.);
#19700=EDGE_CURVE('',#15488,#15488,#12993,.T.);
#19701=EDGE_CURVE('',#15489,#15489,#12994,.T.);
#19702=EDGE_CURVE('',#15490,#15490,#12995,.T.);
#19703=EDGE_CURVE('',#15491,#15491,#12996,.T.);
#19704=EDGE_CURVE('',#15482,#15492,#9338,.T.);
#19705=EDGE_CURVE('',#15492,#15492,#12997,.T.);
#19706=EDGE_CURVE('',#15493,#15493,#12998,.T.);
#19707=EDGE_CURVE('',#15493,#15488,#9339,.T.);
#19708=EDGE_CURVE('',#15493,#15494,#9340,.T.);
#19709=EDGE_CURVE('',#15494,#15494,#12999,.T.);
#19710=EDGE_CURVE('',#15495,#15492,#9341,.T.);
#19711=EDGE_CURVE('',#15496,#15494,#9342,.T.);
#19712=EDGE_CURVE('',#15497,#15497,#13000,.T.);
#19713=EDGE_CURVE('',#15497,#15491,#9343,.T.);
#19714=EDGE_CURVE('',#15497,#15498,#9344,.T.);
#19715=EDGE_CURVE('',#15498,#15498,#13001,.T.);
#19716=EDGE_CURVE('',#15499,#15499,#13002,.T.);
#19717=EDGE_CURVE('',#15499,#15489,#9345,.T.);
#19718=EDGE_CURVE('',#15499,#15500,#9346,.T.);
#19719=EDGE_CURVE('',#15500,#15500,#13003,.T.);
#19720=EDGE_CURVE('',#15501,#15501,#13004,.T.);
#19721=EDGE_CURVE('',#15502,#15502,#13005,.T.);
#19722=EDGE_CURVE('',#15501,#15503,#9347,.T.);
#19723=EDGE_CURVE('',#15503,#15503,#13006,.T.);
#19724=EDGE_CURVE('',#15502,#15504,#9348,.T.);
#19725=EDGE_CURVE('',#15504,#15504,#13007,.T.);
#19726=EDGE_CURVE('',#15505,#15505,#13008,.T.);
#19727=EDGE_CURVE('',#15505,#15506,#9349,.T.);
#19728=EDGE_CURVE('',#15506,#15506,#13009,.T.);
#19729=EDGE_CURVE('',#15507,#15507,#13010,.T.);
#19730=EDGE_CURVE('',#15507,#15505,#9350,.T.);
#19731=EDGE_CURVE('',#15478,#15508,#9351,.T.);
#19732=EDGE_CURVE('',#15509,#15480,#9352,.T.);
#19733=EDGE_CURVE('',#15509,#15510,#9353,.T.);
#19734=EDGE_CURVE('',#15469,#15510,#9354,.T.);
#19735=EDGE_CURVE('',#15511,#15471,#9355,.T.);
#19736=EDGE_CURVE('',#15511,#15508,#9356,.T.);
#19737=EDGE_CURVE('',#15507,#15490,#9357,.T.);
#19738=EDGE_CURVE('',#15508,#15484,#9358,.T.);
#19739=EDGE_CURVE('',#15485,#15511,#9359,.T.);
#19740=EDGE_CURVE('',#15487,#15509,#9360,.T.);
#19741=EDGE_CURVE('',#15510,#15486,#9361,.T.);
#27636=ORIENTED_EDGE('',*,*,#19669,.T.);
#27637=ORIENTED_EDGE('',*,*,#19670,.T.);
#27638=ORIENTED_EDGE('',*,*,#19671,.T.);
#27639=ORIENTED_EDGE('',*,*,#19670,.F.);
#27640=ORIENTED_EDGE('',*,*,#19669,.F.);
#27641=ORIENTED_EDGE('',*,*,#19672,.T.);
#27642=ORIENTED_EDGE('',*,*,#19673,.T.);
#27643=ORIENTED_EDGE('',*,*,#19674,.T.);
#27644=ORIENTED_EDGE('',*,*,#19672,.F.);
#27645=ORIENTED_EDGE('',*,*,#19675,.F.);
#27646=ORIENTED_EDGE('',*,*,#19676,.F.);
#27647=ORIENTED_EDGE('',*,*,#19677,.F.);
#27648=ORIENTED_EDGE('',*,*,#19678,.F.);
#27649=ORIENTED_EDGE('',*,*,#19671,.F.);
#27650=ORIENTED_EDGE('',*,*,#19679,.T.);
#27651=ORIENTED_EDGE('',*,*,#19673,.F.);
#27652=ORIENTED_EDGE('',*,*,#19674,.F.);
#27653=ORIENTED_EDGE('',*,*,#19679,.F.);
#27654=ORIENTED_EDGE('',*,*,#19680,.T.);
#27655=ORIENTED_EDGE('',*,*,#19681,.T.);
#27656=ORIENTED_EDGE('',*,*,#19682,.T.);
#27657=ORIENTED_EDGE('',*,*,#19681,.F.);
#27658=ORIENTED_EDGE('',*,*,#19680,.F.);
#27659=ORIENTED_EDGE('',*,*,#19683,.T.);
#27660=ORIENTED_EDGE('',*,*,#19684,.T.);
#27661=ORIENTED_EDGE('',*,*,#19685,.T.);
#27662=ORIENTED_EDGE('',*,*,#19683,.F.);
#27663=ORIENTED_EDGE('',*,*,#19686,.F.);
#27664=ORIENTED_EDGE('',*,*,#19687,.F.);
#27665=ORIENTED_EDGE('',*,*,#19688,.F.);
#27666=ORIENTED_EDGE('',*,*,#19689,.F.);
#27667=ORIENTED_EDGE('',*,*,#19682,.F.);
#27668=ORIENTED_EDGE('',*,*,#19690,.T.);
#27669=ORIENTED_EDGE('',*,*,#19684,.F.);
#27670=ORIENTED_EDGE('',*,*,#19685,.F.);
#27671=ORIENTED_EDGE('',*,*,#19690,.F.);
#27672=ORIENTED_EDGE('',*,*,#19691,.T.);
#27673=ORIENTED_EDGE('',*,*,#19692,.T.);
#27674=ORIENTED_EDGE('',*,*,#19693,.T.);
#27675=ORIENTED_EDGE('',*,*,#19692,.F.);
#27676=ORIENTED_EDGE('',*,*,#19694,.F.);
#27677=ORIENTED_EDGE('',*,*,#19695,.T.);
#27678=ORIENTED_EDGE('',*,*,#19696,.F.);
#27679=ORIENTED_EDGE('',*,*,#19676,.T.);
#27680=ORIENTED_EDGE('',*,*,#19697,.F.);
#27681=ORIENTED_EDGE('',*,*,#19698,.T.);
#27682=ORIENTED_EDGE('',*,*,#19699,.F.);
#27683=ORIENTED_EDGE('',*,*,#19687,.T.);
#27684=ORIENTED_EDGE('',*,*,#19700,.F.);
#27685=ORIENTED_EDGE('',*,*,#19701,.F.);
#27686=ORIENTED_EDGE('',*,*,#19702,.F.);
#27687=ORIENTED_EDGE('',*,*,#19703,.F.);
#27688=ORIENTED_EDGE('',*,*,#19693,.F.);
#27689=ORIENTED_EDGE('',*,*,#19691,.F.);
#27690=ORIENTED_EDGE('',*,*,#19704,.T.);
#27691=ORIENTED_EDGE('',*,*,#19705,.T.);
#27692=ORIENTED_EDGE('',*,*,#19704,.F.);
#27693=ORIENTED_EDGE('',*,*,#19706,.T.);
#27694=ORIENTED_EDGE('',*,*,#19707,.T.);
#27695=ORIENTED_EDGE('',*,*,#19700,.T.);
#27696=ORIENTED_EDGE('',*,*,#19707,.F.);
#27697=ORIENTED_EDGE('',*,*,#19706,.F.);
#27698=ORIENTED_EDGE('',*,*,#19708,.T.);
#27699=ORIENTED_EDGE('',*,*,#19709,.T.);
#27700=ORIENTED_EDGE('',*,*,#19708,.F.);
#27701=ORIENTED_EDGE('',*,*,#19710,.T.);
#27702=ORIENTED_EDGE('',*,*,#19705,.F.);
#27703=ORIENTED_EDGE('',*,*,#19710,.F.);
#27704=ORIENTED_EDGE('',*,*,#19711,.T.);
#27705=ORIENTED_EDGE('',*,*,#19709,.F.);
#27706=ORIENTED_EDGE('',*,*,#19711,.F.);
#27707=ORIENTED_EDGE('',*,*,#19712,.T.);
#27708=ORIENTED_EDGE('',*,*,#19713,.T.);
#27709=ORIENTED_EDGE('',*,*,#19703,.T.);
#27710=ORIENTED_EDGE('',*,*,#19713,.F.);
#27711=ORIENTED_EDGE('',*,*,#19712,.F.);
#27712=ORIENTED_EDGE('',*,*,#19714,.T.);
#27713=ORIENTED_EDGE('',*,*,#19715,.T.);
#27714=ORIENTED_EDGE('',*,*,#19714,.F.);
#27715=ORIENTED_EDGE('',*,*,#19716,.T.);
#27716=ORIENTED_EDGE('',*,*,#19717,.T.);
#27717=ORIENTED_EDGE('',*,*,#19701,.T.);
#27718=ORIENTED_EDGE('',*,*,#19717,.F.);
#27719=ORIENTED_EDGE('',*,*,#19716,.F.);
#27720=ORIENTED_EDGE('',*,*,#19718,.T.);
#27721=ORIENTED_EDGE('',*,*,#19719,.T.);
#27722=ORIENTED_EDGE('',*,*,#19718,.F.);
#27723=ORIENTED_EDGE('',*,*,#19719,.F.);
#27724=ORIENTED_EDGE('',*,*,#19720,.F.);
#27725=ORIENTED_EDGE('',*,*,#19715,.F.);
#27726=ORIENTED_EDGE('',*,*,#19721,.F.);
#27727=ORIENTED_EDGE('',*,*,#19720,.T.);
#27728=ORIENTED_EDGE('',*,*,#19722,.T.);
#27729=ORIENTED_EDGE('',*,*,#19723,.F.);
#27730=ORIENTED_EDGE('',*,*,#19722,.F.);
#27731=ORIENTED_EDGE('',*,*,#19721,.T.);
#27732=ORIENTED_EDGE('',*,*,#19724,.T.);
#27733=ORIENTED_EDGE('',*,*,#19725,.F.);
#27734=ORIENTED_EDGE('',*,*,#19724,.F.);
#27735=ORIENTED_EDGE('',*,*,#19726,.T.);
#27736=ORIENTED_EDGE('',*,*,#19727,.T.);
#27737=ORIENTED_EDGE('',*,*,#19728,.T.);
#27738=ORIENTED_EDGE('',*,*,#19727,.F.);
#27739=ORIENTED_EDGE('',*,*,#19729,.F.);
#27740=ORIENTED_EDGE('',*,*,#19730,.T.);
#27741=ORIENTED_EDGE('',*,*,#19726,.F.);
#27742=ORIENTED_EDGE('',*,*,#19730,.F.);
#27743=ORIENTED_EDGE('',*,*,#19731,.F.);
#27744=ORIENTED_EDGE('',*,*,#19689,.T.);
#27745=ORIENTED_EDGE('',*,*,#19732,.F.);
#27746=ORIENTED_EDGE('',*,*,#19733,.T.);
#27747=ORIENTED_EDGE('',*,*,#19734,.F.);
#27748=ORIENTED_EDGE('',*,*,#19678,.T.);
#27749=ORIENTED_EDGE('',*,*,#19735,.F.);
#27750=ORIENTED_EDGE('',*,*,#19736,.T.);
#27751=ORIENTED_EDGE('',*,*,#19723,.T.);
#27752=ORIENTED_EDGE('',*,*,#19725,.T.);
#27753=ORIENTED_EDGE('',*,*,#19728,.F.);
#27754=ORIENTED_EDGE('',*,*,#19729,.T.);
#27755=ORIENTED_EDGE('',*,*,#19737,.T.);
#27756=ORIENTED_EDGE('',*,*,#19702,.T.);
#27757=ORIENTED_EDGE('',*,*,#19737,.F.);
#27758=ORIENTED_EDGE('',*,*,#19731,.T.);
#27759=ORIENTED_EDGE('',*,*,#19738,.T.);
#27760=ORIENTED_EDGE('',*,*,#19694,.T.);
#27761=ORIENTED_EDGE('',*,*,#19686,.T.);
#27762=ORIENTED_EDGE('',*,*,#19738,.F.);
#27763=ORIENTED_EDGE('',*,*,#19736,.F.);
#27764=ORIENTED_EDGE('',*,*,#19739,.F.);
#27765=ORIENTED_EDGE('',*,*,#19695,.F.);
#27766=ORIENTED_EDGE('',*,*,#19732,.T.);
#27767=ORIENTED_EDGE('',*,*,#19688,.T.);
#27768=ORIENTED_EDGE('',*,*,#19699,.T.);
#27769=ORIENTED_EDGE('',*,*,#19740,.T.);
#27770=ORIENTED_EDGE('',*,*,#19740,.F.);
#27771=ORIENTED_EDGE('',*,*,#19698,.F.);
#27772=ORIENTED_EDGE('',*,*,#19741,.F.);
#27773=ORIENTED_EDGE('',*,*,#19733,.F.);
#27774=ORIENTED_EDGE('',*,*,#19734,.T.);
#27775=ORIENTED_EDGE('',*,*,#19741,.T.);
#27776=ORIENTED_EDGE('',*,*,#19697,.T.);
#27777=ORIENTED_EDGE('',*,*,#19675,.T.);
#27778=ORIENTED_EDGE('',*,*,#19735,.T.);
#27779=ORIENTED_EDGE('',*,*,#19677,.T.);
#27780=ORIENTED_EDGE('',*,*,#19696,.T.);
#27781=ORIENTED_EDGE('',*,*,#19739,.T.);
#30298=CONICAL_SURFACE('',#33494,1.125,0.785398163397452);
#30299=CONICAL_SURFACE('',#33501,1.05,1.02974425867665);
#30300=CONICAL_SURFACE('',#33502,1.125,0.785398163397452);
#30301=CONICAL_SURFACE('',#33509,0.525,1.02974425867665);
#30302=CONICAL_SURFACE('',#33510,1.65,0.785398163397448);
#30303=CONICAL_SURFACE('',#33520,1.65,0.785398163397448);
#30304=CONICAL_SURFACE('',#33524,0.775000000000001,1.02974425867666);
#30305=CONICAL_SURFACE('',#33525,0.775,1.02974425867666);
#30306=CONICAL_SURFACE('',#33526,3.15,0.785398163397448);
#30307=CONICAL_SURFACE('',#33530,3.15,0.785398163397448);
#30308=CONICAL_SURFACE('',#33542,2.165,0.785398163397448);
#30309=CONICAL_SURFACE('',#33548,2.165,0.785398163397448);
#31624=ADVANCED_FACE('',(#4649),#30298,.F.);
#31625=ADVANCED_FACE('',(#4650),#1881,.F.);
#31626=ADVANCED_FACE('',(#4651,#2215),#3064,.T.);
#31627=ADVANCED_FACE('',(#4652),#30299,.F.);
#31628=ADVANCED_FACE('',(#4653),#30300,.F.);
#31629=ADVANCED_FACE('',(#4654),#1882,.F.);
#31630=ADVANCED_FACE('',(#4655,#2216),#3065,.T.);
#31631=ADVANCED_FACE('',(#4656),#30301,.F.);
#31632=ADVANCED_FACE('',(#4657),#30302,.F.);
#31633=ADVANCED_FACE('',(#4658,#2217,#2218,#2219,#2220,#2221),#3066,.F.);
#31634=ADVANCED_FACE('',(#4659),#1883,.F.);
#31635=ADVANCED_FACE('',(#4660),#30303,.F.);
#31636=ADVANCED_FACE('',(#4661),#1884,.F.);
#31637=ADVANCED_FACE('',(#4662),#30304,.F.);
#31638=ADVANCED_FACE('',(#4663),#30305,.F.);
#31639=ADVANCED_FACE('',(#4664),#30306,.F.);
#31640=ADVANCED_FACE('',(#4665),#1885,.F.);
#31641=ADVANCED_FACE('',(#4666),#30307,.F.);
#31642=ADVANCED_FACE('',(#4667),#1886,.F.);
#31643=ADVANCED_FACE('',(#4668,#2222),#3067,.F.);
#31644=ADVANCED_FACE('',(#4669,#2223),#3068,.F.);
#31645=ADVANCED_FACE('',(#4670),#1887,.F.);
#31646=ADVANCED_FACE('',(#4671),#1888,.F.);
#31647=ADVANCED_FACE('',(#4672),#30308,.F.);
#31648=ADVANCED_FACE('',(#4673),#1889,.F.);
#31649=ADVANCED_FACE('',(#4674,#2224,#2225,#2226),#3069,.T.);
#31650=ADVANCED_FACE('',(#4675),#30309,.F.);
#31651=ADVANCED_FACE('',(#4676),#3070,.T.);
#31652=ADVANCED_FACE('',(#4677),#3071,.T.);
#31653=ADVANCED_FACE('',(#4678),#3072,.T.);
#31654=ADVANCED_FACE('',(#4679),#3073,.T.);
#31655=ADVANCED_FACE('',(#4680),#3074,.T.);
#31656=ADVANCED_FACE('',(#4681),#3075,.T.);
#32084=CLOSED_SHELL('',(#31624,#31625,#31626,#31627,#31628,#31629,#31630,
#31631,#31632,#31633,#31634,#31635,#31636,#31637,#31638,#31639,#31640,#31641,
#31642,#31643,#31644,#31645,#31646,#31647,#31648,#31649,#31650,#31651,#31652,
#31653,#31654,#31655,#31656));
#33493=AXIS2_PLACEMENT_3D('',#84179,#38993,#38994);
#33494=AXIS2_PLACEMENT_3D('',#84180,#38995,#38996);
#33495=AXIS2_PLACEMENT_3D('',#84182,#38997,#38998);
#33496=AXIS2_PLACEMENT_3D('',#84185,#39000,#39001);
#33497=AXIS2_PLACEMENT_3D('',#84186,#39002,#39003);
#33498=AXIS2_PLACEMENT_3D('',#84190,#39005,#39006);
#33499=AXIS2_PLACEMENT_3D('',#84191,#39007,#39008);
#33500=AXIS2_PLACEMENT_3D('',#84192,#39009,#39010);
#33501=AXIS2_PLACEMENT_3D('',#84201,#39015,#39016);
#33502=AXIS2_PLACEMENT_3D('',#84204,#39018,#39019);
#33503=AXIS2_PLACEMENT_3D('',#84206,#39020,#39021);
#33504=AXIS2_PLACEMENT_3D('',#84209,#39023,#39024);
#33505=AXIS2_PLACEMENT_3D('',#84210,#39025,#39026);
#33506=AXIS2_PLACEMENT_3D('',#84214,#39028,#39029);
#33507=AXIS2_PLACEMENT_3D('',#84215,#39030,#39031);
#33508=AXIS2_PLACEMENT_3D('',#84216,#39032,#39033);
#33509=AXIS2_PLACEMENT_3D('',#84225,#39038,#39039);
#33510=AXIS2_PLACEMENT_3D('',#84228,#39041,#39042);
#33511=AXIS2_PLACEMENT_3D('',#84230,#39043,#39044);
#33512=AXIS2_PLACEMENT_3D('',#84233,#39046,#39047);
#33513=AXIS2_PLACEMENT_3D('',#84234,#39048,#39049);
#33514=AXIS2_PLACEMENT_3D('',#84246,#39056,#39057);
#33515=AXIS2_PLACEMENT_3D('',#84248,#39058,#39059);
#33516=AXIS2_PLACEMENT_3D('',#84250,#39060,#39061);
#33517=AXIS2_PLACEMENT_3D('',#84252,#39062,#39063);
#33518=AXIS2_PLACEMENT_3D('',#84253,#39064,#39065);
#33519=AXIS2_PLACEMENT_3D('',#84256,#39067,#39068);
#33520=AXIS2_PLACEMENT_3D('',#84257,#39069,#39070);
#33521=AXIS2_PLACEMENT_3D('',#84259,#39071,#39072);
#33522=AXIS2_PLACEMENT_3D('',#84261,#39074,#39075);
#33523=AXIS2_PLACEMENT_3D('',#84264,#39077,#39078);
#33524=AXIS2_PLACEMENT_3D('',#84265,#39079,#39080);
#33525=AXIS2_PLACEMENT_3D('',#84268,#39082,#39083);
#33526=AXIS2_PLACEMENT_3D('',#84271,#39085,#39086);
#33527=AXIS2_PLACEMENT_3D('',#84273,#39087,#39088);
#33528=AXIS2_PLACEMENT_3D('',#84275,#39090,#39091);
#33529=AXIS2_PLACEMENT_3D('',#84278,#39093,#39094);
#33530=AXIS2_PLACEMENT_3D('',#84279,#39095,#39096);
#33531=AXIS2_PLACEMENT_3D('',#84281,#39097,#39098);
#33532=AXIS2_PLACEMENT_3D('',#84283,#39100,#39101);
#33533=AXIS2_PLACEMENT_3D('',#84286,#39103,#39104);
#33534=AXIS2_PLACEMENT_3D('',#84287,#39105,#39106);
#33535=AXIS2_PLACEMENT_3D('',#84289,#39107,#39108);
#33536=AXIS2_PLACEMENT_3D('',#84290,#39109,#39110);
#33537=AXIS2_PLACEMENT_3D('',#84292,#39111,#39112);
#33538=AXIS2_PLACEMENT_3D('',#84293,#39113,#39114);
#33539=AXIS2_PLACEMENT_3D('',#84296,#39116,#39117);
#33540=AXIS2_PLACEMENT_3D('',#84297,#39118,#39119);
#33541=AXIS2_PLACEMENT_3D('',#84300,#39121,#39122);
#33542=AXIS2_PLACEMENT_3D('',#84301,#39123,#39124);
#33543=AXIS2_PLACEMENT_3D('',#84303,#39125,#39126);
#33544=AXIS2_PLACEMENT_3D('',#84306,#39128,#39129);
#33545=AXIS2_PLACEMENT_3D('',#84307,#39130,#39131);
#33546=AXIS2_PLACEMENT_3D('',#84309,#39132,#39133);
#33547=AXIS2_PLACEMENT_3D('',#84311,#39135,#39136);
#33548=AXIS2_PLACEMENT_3D('',#84322,#39143,#39144);
#33549=AXIS2_PLACEMENT_3D('',#84324,#39146,#39147);
#33550=AXIS2_PLACEMENT_3D('',#84326,#39149,#39150);
#33551=AXIS2_PLACEMENT_3D('',#84328,#39152,#39153);
#33552=AXIS2_PLACEMENT_3D('',#84330,#39155,#39156);
#33553=AXIS2_PLACEMENT_3D('',#84332,#39158,#39159);
#33554=AXIS2_PLACEMENT_3D('',#84333,#39160,#39161);
#38993=DIRECTION('axis',(0.,0.,1.));
#38994=DIRECTION('refdir',(1.,0.,0.));
#38995=DIRECTION('center_axis',(-1.,0.,0.));
#38996=DIRECTION('ref_axis',(0.,0.,-1.));
#38997=DIRECTION('center_axis',(1.,0.,0.));
#38998=DIRECTION('ref_axis',(0.,0.,-1.));
#38999=DIRECTION('',(-0.707106781186545,8.65956056235497E-17,0.70710678118655));
#39000=DIRECTION('center_axis',(-1.,0.,0.));
#39001=DIRECTION('ref_axis',(0.,0.,-1.));
#39002=DIRECTION('center_axis',(1.,0.,0.));
#39003=DIRECTION('ref_axis',(0.,0.,-1.));
#39004=DIRECTION('',(1.,0.,0.));
#39005=DIRECTION('center_axis',(1.,0.,0.));
#39006=DIRECTION('ref_axis',(0.,0.,-1.));
#39007=DIRECTION('center_axis',(1.,0.,0.));
#39008=DIRECTION('ref_axis',(0.,0.,-1.));
#39009=DIRECTION('center_axis',(-1.,0.,0.));
#39010=DIRECTION('ref_axis',(0.,0.,1.));
#39011=DIRECTION('',(0.,1.,0.));
#39012=DIRECTION('',(0.,0.,-1.));
#39013=DIRECTION('',(0.,-1.,0.));
#39014=DIRECTION('',(0.,0.,1.));
#39015=DIRECTION('center_axis',(-1.,0.,0.));
#39016=DIRECTION('ref_axis',(0.,1.,0.));
#39017=DIRECTION('',(-0.515038074910058,-0.85716730070211,1.04972719113862E-16));
#39018=DIRECTION('center_axis',(1.,0.,0.));
#39019=DIRECTION('ref_axis',(0.,0.,-1.));
#39020=DIRECTION('center_axis',(-1.,0.,0.));
#39021=DIRECTION('ref_axis',(0.,0.,-1.));
#39022=DIRECTION('',(0.707106781186545,-8.65956056235497E-17,0.70710678118655));
#39023=DIRECTION('center_axis',(1.,0.,0.));
#39024=DIRECTION('ref_axis',(0.,0.,-1.));
#39025=DIRECTION('center_axis',(-1.,0.,0.));
#39026=DIRECTION('ref_axis',(0.,0.,-1.));
#39027=DIRECTION('',(-1.,0.,0.));
#39028=DIRECTION('center_axis',(-1.,0.,0.));
#39029=DIRECTION('ref_axis',(0.,0.,-1.));
#39030=DIRECTION('center_axis',(-1.,0.,0.));
#39031=DIRECTION('ref_axis',(0.,0.,-1.));
#39032=DIRECTION('center_axis',(1.,0.,0.));
#39033=DIRECTION('ref_axis',(0.,0.,-1.));
#39034=DIRECTION('',(0.,1.,0.));
#39035=DIRECTION('',(0.,0.,1.));
#39036=DIRECTION('',(0.,-1.,0.));
#39037=DIRECTION('',(0.,0.,-1.));
#39038=DIRECTION('center_axis',(1.,0.,0.));
#39039=DIRECTION('ref_axis',(0.,1.,0.));
#39040=DIRECTION('',(0.515038074910058,-0.85716730070211,-1.04972719113862E-16));
#39041=DIRECTION('center_axis',(0.,-1.,0.));
#39042=DIRECTION('ref_axis',(1.,0.,0.));
#39043=DIRECTION('center_axis',(0.,1.,0.));
#39044=DIRECTION('ref_axis',(1.,0.,0.));
#39045=DIRECTION('',(-0.707106781186547,-0.707106781186548,-8.65956056235493E-17));
#39046=DIRECTION('center_axis',(0.,-1.,0.));
#39047=DIRECTION('ref_axis',(1.,0.,0.));
#39048=DIRECTION('center_axis',(0.,1.,0.));
#39049=DIRECTION('ref_axis',(1.,0.,0.));
#39050=DIRECTION('',(0.707106781186547,0.,-0.707106781186547));
#39051=DIRECTION('',(-1.,0.,0.));
#39052=DIRECTION('',(0.707106781186546,0.,0.707106781186549));
#39053=DIRECTION('',(-0.707106781186546,0.,0.707106781186549));
#39054=DIRECTION('',(1.,0.,0.));
#39055=DIRECTION('',(-0.707106781186546,0.,-0.707106781186549));
#39056=DIRECTION('center_axis',(0.,-1.,0.));
#39057=DIRECTION('ref_axis',(1.,0.,0.));
#39058=DIRECTION('center_axis',(0.,-1.,0.));
#39059=DIRECTION('ref_axis',(1.,0.,0.));
#39060=DIRECTION('center_axis',(0.,-1.,0.));
#39061=DIRECTION('ref_axis',(1.,0.,0.));
#39062=DIRECTION('center_axis',(0.,-1.,0.));
#39063=DIRECTION('ref_axis',(1.,0.,0.));
#39064=DIRECTION('center_axis',(0.,1.,0.));
#39065=DIRECTION('ref_axis',(1.,0.,0.));
#39066=DIRECTION('',(0.,1.,0.));
#39067=DIRECTION('center_axis',(0.,1.,0.));
#39068=DIRECTION('ref_axis',(1.,0.,0.));
#39069=DIRECTION('center_axis',(0.,-1.,0.));
#39070=DIRECTION('ref_axis',(1.,0.,0.));
#39071=DIRECTION('center_axis',(0.,1.,0.));
#39072=DIRECTION('ref_axis',(1.,0.,0.));
#39073=DIRECTION('',(-0.707106781186547,-0.707106781186548,-8.65956056235493E-17));
#39074=DIRECTION('center_axis',(0.,1.,0.));
#39075=DIRECTION('ref_axis',(1.,0.,0.));
#39076=DIRECTION('',(0.,1.,0.));
#39077=DIRECTION('center_axis',(0.,1.,0.));
#39078=DIRECTION('ref_axis',(1.,0.,0.));
#39079=DIRECTION('center_axis',(0.,-1.,0.));
#39080=DIRECTION('ref_axis',(1.,0.,0.));
#39081=DIRECTION('',(-0.857167300702115,-0.515038074910049,-1.04972719113862E-16));
#39082=DIRECTION('center_axis',(0.,-1.,0.));
#39083=DIRECTION('ref_axis',(1.,0.,0.));
#39084=DIRECTION('',(-0.857167300702115,-0.515038074910049,-1.04972719113862E-16));
#39085=DIRECTION('center_axis',(0.,-1.,0.));
#39086=DIRECTION('ref_axis',(1.,0.,0.));
#39087=DIRECTION('center_axis',(0.,1.,0.));
#39088=DIRECTION('ref_axis',(1.,0.,0.));
#39089=DIRECTION('',(-0.707106781186547,-0.707106781186548,-8.65956056235493E-17));
#39090=DIRECTION('center_axis',(0.,1.,0.));
#39091=DIRECTION('ref_axis',(1.,0.,0.));
#39092=DIRECTION('',(0.,1.,0.));
#39093=DIRECTION('center_axis',(0.,1.,0.));
#39094=DIRECTION('ref_axis',(1.,0.,0.));
#39095=DIRECTION('center_axis',(0.,-1.,0.));
#39096=DIRECTION('ref_axis',(1.,0.,0.));
#39097=DIRECTION('center_axis',(0.,1.,0.));
#39098=DIRECTION('ref_axis',(1.,0.,0.));
#39099=DIRECTION('',(-0.707106781186547,-0.707106781186548,-8.65956056235493E-17));
#39100=DIRECTION('center_axis',(0.,1.,0.));
#39101=DIRECTION('ref_axis',(1.,0.,0.));
#39102=DIRECTION('',(0.,1.,0.));
#39103=DIRECTION('center_axis',(0.,1.,0.));
#39104=DIRECTION('ref_axis',(1.,0.,0.));
#39105=DIRECTION('center_axis',(0.,1.,0.));
#39106=DIRECTION('ref_axis',(1.,0.,0.));
#39107=DIRECTION('center_axis',(0.,-1.,0.));
#39108=DIRECTION('ref_axis',(1.,0.,0.));
#39109=DIRECTION('center_axis',(0.,1.,0.));
#39110=DIRECTION('ref_axis',(1.,0.,0.));
#39111=DIRECTION('center_axis',(0.,-1.,0.));
#39112=DIRECTION('ref_axis',(1.,0.,0.));
#39113=DIRECTION('center_axis',(0.,1.,0.));
#39114=DIRECTION('ref_axis',(1.,0.,0.));
#39115=DIRECTION('',(0.,1.,0.));
#39116=DIRECTION('center_axis',(0.,-1.,0.));
#39117=DIRECTION('ref_axis',(1.,0.,0.));
#39118=DIRECTION('center_axis',(0.,1.,0.));
#39119=DIRECTION('ref_axis',(1.,0.,0.));
#39120=DIRECTION('',(0.,1.,0.));
#39121=DIRECTION('center_axis',(0.,-1.,0.));
#39122=DIRECTION('ref_axis',(1.,0.,0.));
#39123=DIRECTION('center_axis',(0.,1.,0.));
#39124=DIRECTION('ref_axis',(1.,0.,0.));
#39125=DIRECTION('center_axis',(0.,-1.,0.));
#39126=DIRECTION('ref_axis',(1.,0.,0.));
#39127=DIRECTION('',(-0.707106781186547,0.707106781186548,8.65956056235493E-17));
#39128=DIRECTION('center_axis',(0.,1.,0.));
#39129=DIRECTION('ref_axis',(1.,0.,0.));
#39130=DIRECTION('center_axis',(0.,1.,0.));
#39131=DIRECTION('ref_axis',(1.,0.,0.));
#39132=DIRECTION('center_axis',(0.,1.,0.));
#39133=DIRECTION('ref_axis',(1.,0.,0.));
#39134=DIRECTION('',(0.,1.,0.));
#39135=DIRECTION('center_axis',(0.,1.,0.));
#39136=DIRECTION('ref_axis',(0.,0.,1.));
#39137=DIRECTION('',(-0.707106781186547,0.,0.707106781186547));
#39138=DIRECTION('',(0.707106781186546,0.,0.707106781186549));
#39139=DIRECTION('',(-1.,0.,0.));
#39140=DIRECTION('',(0.707106781186546,0.,-0.707106781186549));
#39141=DIRECTION('',(-0.707106781186546,0.,-0.707106781186549));
#39142=DIRECTION('',(1.,0.,0.));
#39143=DIRECTION('center_axis',(0.,-1.,0.));
#39144=DIRECTION('ref_axis',(1.,0.,0.));
#39145=DIRECTION('',(-0.707106781186547,-0.707106781186548,-8.65956056235493E-17));
#39146=DIRECTION('center_axis',(0.707106781186548,0.,0.707106781186548));
#39147=DIRECTION('ref_axis',(0.707106781186548,0.,-0.707106781186548));
#39148=DIRECTION('',(0.,-1.,0.));
#39149=DIRECTION('center_axis',(0.,0.,1.));
#39150=DIRECTION('ref_axis',(1.,0.,0.));
#39151=DIRECTION('',(0.,1.,0.));
#39152=DIRECTION('center_axis',(0.707106781186549,0.,-0.707106781186546));
#39153=DIRECTION('ref_axis',(-0.707106781186546,0.,-0.707106781186549));
#39154=DIRECTION('',(0.,1.,0.));
#39155=DIRECTION('center_axis',(0.,0.,-1.));
#39156=DIRECTION('ref_axis',(-1.,0.,0.));
#39157=DIRECTION('',(0.,-1.,0.));
#39158=DIRECTION('center_axis',(-0.707106781186549,0.,-0.707106781186546));
#39159=DIRECTION('ref_axis',(-0.707106781186546,0.,0.707106781186549));
#39160=DIRECTION('center_axis',(-0.707106781186549,0.,0.707106781186546));
#39161=DIRECTION('ref_axis',(0.707106781186546,0.,0.707106781186549));
#84179=CARTESIAN_POINT('',(0.,0.,0.));
#84180=CARTESIAN_POINT('Origin',(-17.425,15.,5.5));
#84181=CARTESIAN_POINT('',(-17.35,15.,6.55));
#84182=CARTESIAN_POINT('Origin',(-17.35,15.,5.5));
#84183=CARTESIAN_POINT('',(-17.5,15.,6.7));
#84184=CARTESIAN_POINT('',(-17.425,15.,6.625));
#84185=CARTESIAN_POINT('Origin',(-17.5,15.,5.5));
#84186=CARTESIAN_POINT('Origin',(-17.5,15.,5.5));
#84187=CARTESIAN_POINT('',(-13.5,15.,6.55));
#84188=CARTESIAN_POINT('',(-17.5,15.,6.55));
#84189=CARTESIAN_POINT('',(-13.5,13.95,5.5));
#84190=CARTESIAN_POINT('Origin',(-13.5,15.,5.5));
#84191=CARTESIAN_POINT('Origin',(-13.5,15.,5.5));
#84192=CARTESIAN_POINT('Origin',(-17.5,10.,0.));
#84193=CARTESIAN_POINT('',(-17.5,10.,0.5));
#84194=CARTESIAN_POINT('',(-17.5,20.,0.5));
#84195=CARTESIAN_POINT('',(-17.5,10.,0.5));
#84196=CARTESIAN_POINT('',(-17.5,10.,15.5));
#84197=CARTESIAN_POINT('',(-17.5,10.,16.));
#84198=CARTESIAN_POINT('',(-17.5,20.,15.5));
#84199=CARTESIAN_POINT('',(-17.5,10.,15.5));
#84200=CARTESIAN_POINT('',(-17.5,20.,16.));
#84201=CARTESIAN_POINT('Origin',(-13.5,15.,5.5));
#84202=CARTESIAN_POINT('',(-12.8690963500211,15.,5.5));
#84203=CARTESIAN_POINT('',(-13.5,13.95,5.5));
#84204=CARTESIAN_POINT('Origin',(17.425,15.,5.5));
#84205=CARTESIAN_POINT('',(17.35,15.,6.55));
#84206=CARTESIAN_POINT('Origin',(17.35,15.,5.5));
#84207=CARTESIAN_POINT('',(17.5,15.,6.7));
#84208=CARTESIAN_POINT('',(17.425,15.,6.625));
#84209=CARTESIAN_POINT('Origin',(17.5,15.,5.5));
#84210=CARTESIAN_POINT('Origin',(17.5,15.,5.5));
#84211=CARTESIAN_POINT('',(13.5,15.,6.55));
#84212=CARTESIAN_POINT('',(17.5,15.,6.55));
#84213=CARTESIAN_POINT('',(13.5,13.95,5.5));
#84214=CARTESIAN_POINT('Origin',(13.5,15.,5.5));
#84215=CARTESIAN_POINT('Origin',(13.5,15.,5.5));
#84216=CARTESIAN_POINT('Origin',(17.5,10.,16.));
#84217=CARTESIAN_POINT('',(17.5,10.,15.5));
#84218=CARTESIAN_POINT('',(17.5,20.,15.5));
#84219=CARTESIAN_POINT('',(17.5,10.,15.5));
#84220=CARTESIAN_POINT('',(17.5,10.,0.5));
#84221=CARTESIAN_POINT('',(17.5,10.,0.));
#84222=CARTESIAN_POINT('',(17.5,20.,0.5));
#84223=CARTESIAN_POINT('',(17.5,10.,0.5));
#84224=CARTESIAN_POINT('',(17.5,20.,0.));
#84225=CARTESIAN_POINT('Origin',(13.1845481750105,15.,5.5));
#84226=CARTESIAN_POINT('',(12.8690963500211,15.,5.5));
#84227=CARTESIAN_POINT('',(13.1845481750105,14.475,5.5));
#84228=CARTESIAN_POINT('Origin',(10.,10.1,11.));
#84229=CARTESIAN_POINT('',(8.45,10.2,11.));
#84230=CARTESIAN_POINT('Origin',(10.,10.2,11.));
#84231=CARTESIAN_POINT('',(8.25,10.,11.));
#84232=CARTESIAN_POINT('',(8.35,10.1,11.));
#84233=CARTESIAN_POINT('Origin',(10.,10.,11.));
#84234=CARTESIAN_POINT('Origin',(0.,10.,8.));
#84235=CARTESIAN_POINT('',(17.,10.,16.));
#84236=CARTESIAN_POINT('',(14.875,10.,18.125));
#84237=CARTESIAN_POINT('',(-17.,10.,16.));
#84238=CARTESIAN_POINT('',(17.5,10.,16.));
#84239=CARTESIAN_POINT('',(-14.875,10.,18.125));
#84240=CARTESIAN_POINT('',(-17.,10.,0.));
#84241=CARTESIAN_POINT('',(-14.875,10.,-2.12499999999999));
#84242=CARTESIAN_POINT('',(17.,10.,0.));
#84243=CARTESIAN_POINT('',(-17.5,10.,0.));
#84244=CARTESIAN_POINT('',(14.875,10.,-2.12499999999999));
#84245=CARTESIAN_POINT('',(-11.75,10.,11.));
#84246=CARTESIAN_POINT('Origin',(-10.,10.,11.));
#84247=CARTESIAN_POINT('',(-13.3,10.,3.5));
#84248=CARTESIAN_POINT('Origin',(-10.,10.,3.5));
#84249=CARTESIAN_POINT('',(-2.315,10.,13.3));
#84250=CARTESIAN_POINT('Origin',(0.,10.,13.3));
#84251=CARTESIAN_POINT('',(6.7,10.,3.5));
#84252=CARTESIAN_POINT('Origin',(10.,10.,3.5));
#84253=CARTESIAN_POINT('Origin',(10.,10.,11.));
#84254=CARTESIAN_POINT('',(8.45,16.,11.));
#84255=CARTESIAN_POINT('',(8.45,10.,11.));
#84256=CARTESIAN_POINT('Origin',(10.,16.,11.));
#84257=CARTESIAN_POINT('Origin',(-10.,10.1,11.));
#84258=CARTESIAN_POINT('',(-11.55,10.2,11.));
#84259=CARTESIAN_POINT('Origin',(-10.,10.2,11.));
#84260=CARTESIAN_POINT('',(-11.65,10.1,11.));
#84261=CARTESIAN_POINT('Origin',(-10.,10.,11.));
#84262=CARTESIAN_POINT('',(-11.55,16.,11.));
#84263=CARTESIAN_POINT('',(-11.55,10.,11.));
#84264=CARTESIAN_POINT('Origin',(-10.,16.,11.));
#84265=CARTESIAN_POINT('Origin',(10.,16.4656669797464,11.));
#84266=CARTESIAN_POINT('',(10.,16.9313339594927,11.));
#84267=CARTESIAN_POINT('',(9.225,16.4656669797464,11.));
#84268=CARTESIAN_POINT('Origin',(-10.,16.4656669797464,11.));
#84269=CARTESIAN_POINT('',(-10.,16.9313339594927,11.));
#84270=CARTESIAN_POINT('',(-10.775,16.4656669797464,11.));
#84271=CARTESIAN_POINT('Origin',(10.,10.15,3.5));
#84272=CARTESIAN_POINT('',(7.,10.3,3.5));
#84273=CARTESIAN_POINT('Origin',(10.,10.3,3.5));
#84274=CARTESIAN_POINT('',(6.85,10.15,3.5));
#84275=CARTESIAN_POINT('Origin',(10.,10.,3.5));
#84276=CARTESIAN_POINT('',(7.,13.2,3.5));
#84277=CARTESIAN_POINT('',(7.,10.,3.5));
#84278=CARTESIAN_POINT('Origin',(10.,13.2,3.5));
#84279=CARTESIAN_POINT('Origin',(-10.,10.15,3.5));
#84280=CARTESIAN_POINT('',(-13.,10.3,3.5));
#84281=CARTESIAN_POINT('Origin',(-10.,10.3,3.5));
#84282=CARTESIAN_POINT('',(-13.15,10.15,3.5));
#84283=CARTESIAN_POINT('Origin',(-10.,10.,3.5));
#84284=CARTESIAN_POINT('',(-13.,13.2,3.5));
#84285=CARTESIAN_POINT('',(-13.,10.,3.5));
#84286=CARTESIAN_POINT('Origin',(-10.,13.2,3.5));
#84287=CARTESIAN_POINT('Origin',(-10.,13.2,3.5));
#84288=CARTESIAN_POINT('',(-11.7,13.2,3.5));
#84289=CARTESIAN_POINT('Origin',(-10.,13.2,3.5));
#84290=CARTESIAN_POINT('Origin',(10.,13.2,3.5));
#84291=CARTESIAN_POINT('',(8.3,13.2,3.5));
#84292=CARTESIAN_POINT('Origin',(10.,13.2,3.5));
#84293=CARTESIAN_POINT('Origin',(-10.,10.,3.5));
#84294=CARTESIAN_POINT('',(-11.7,20.,3.5));
#84295=CARTESIAN_POINT('',(-11.7,10.,3.5));
#84296=CARTESIAN_POINT('Origin',(-10.,20.,3.5));
#84297=CARTESIAN_POINT('Origin',(10.,10.,3.5));
#84298=CARTESIAN_POINT('',(8.3,20.,3.5));
#84299=CARTESIAN_POINT('',(8.3,10.,3.5));
#84300=CARTESIAN_POINT('Origin',(10.,20.,3.5));
#84301=CARTESIAN_POINT('Origin',(0.,19.85,13.3));
#84302=CARTESIAN_POINT('',(-2.015,19.7,13.3));
#84303=CARTESIAN_POINT('Origin',(0.,19.7,13.3));
#84304=CARTESIAN_POINT('',(-2.315,20.,13.3));
#84305=CARTESIAN_POINT('',(-2.165,19.85,13.3));
#84306=CARTESIAN_POINT('Origin',(0.,20.,13.3));
#84307=CARTESIAN_POINT('Origin',(0.,10.,13.3));
#84308=CARTESIAN_POINT('',(-2.015,10.3,13.3));
#84309=CARTESIAN_POINT('Origin',(0.,10.3,13.3));
#84310=CARTESIAN_POINT('',(-2.015,10.,13.3));
#84311=CARTESIAN_POINT('Origin',(0.,20.,8.));
#84312=CARTESIAN_POINT('',(17.,20.,16.));
#84313=CARTESIAN_POINT('',(14.875,20.,18.125));
#84314=CARTESIAN_POINT('',(17.,20.,0.));
#84315=CARTESIAN_POINT('',(14.875,20.,-2.12499999999999));
#84316=CARTESIAN_POINT('',(-17.,20.,0.));
#84317=CARTESIAN_POINT('',(-17.5,20.,0.));
#84318=CARTESIAN_POINT('',(-14.875,20.,-2.12499999999999));
#84319=CARTESIAN_POINT('',(-17.,20.,16.));
#84320=CARTESIAN_POINT('',(-14.875,20.,18.125));
#84321=CARTESIAN_POINT('',(17.5,20.,16.));
#84322=CARTESIAN_POINT('Origin',(0.,10.15,13.3));
#84323=CARTESIAN_POINT('',(-2.165,10.15,13.3));
#84324=CARTESIAN_POINT('Origin',(17.25,10.,15.75));
#84325=CARTESIAN_POINT('',(17.,10.,16.));
#84326=CARTESIAN_POINT('Origin',(-17.5,10.,16.));
#84327=CARTESIAN_POINT('',(-17.,10.,16.));
#84328=CARTESIAN_POINT('Origin',(17.25,10.,0.25));
#84329=CARTESIAN_POINT('',(17.,10.,0.));
#84330=CARTESIAN_POINT('Origin',(17.5,10.,0.));
#84331=CARTESIAN_POINT('',(-17.,10.,0.));
#84332=CARTESIAN_POINT('Origin',(-17.25,10.,0.25));
#84333=CARTESIAN_POINT('Origin',(-17.25,10.,15.75));
#135263=UNCERTAINTY_MEASURE_WITH_UNIT(LENGTH_MEASURE(0.01),#135283,
'DISTANCE_ACCURACY_VALUE',
'Maximum model space distance between geometric entities at asserted c
onnectivities');
#135267=UNCERTAINTY_MEASURE_WITH_UNIT(LENGTH_MEASURE(0.01),#135283,
'DISTANCE_ACCURACY_VALUE',
'Maximum model space distance between geometric entities at asserted c
onnectivities');
#135278=(
GEOMETRIC_REPRESENTATION_CONTEXT(3)
GLOBAL_UNCERTAINTY_ASSIGNED_CONTEXT((#135263))
GLOBAL_UNIT_ASSIGNED_CONTEXT((#135283,#135285,#135286))
REPRESENTATION_CONTEXT('','3D')
);
#135282=(
GEOMETRIC_REPRESENTATION_CONTEXT(3)
GLOBAL_UNCERTAINTY_ASSIGNED_CONTEXT((#135267))
GLOBAL_UNIT_ASSIGNED_CONTEXT((#135283,#135285,#135286))
REPRESENTATION_CONTEXT('','3D')
);
#135283=(
LENGTH_UNIT()
NAMED_UNIT(*)
SI_UNIT(.MILLI.,.METRE.)
);
#135285=(
NAMED_UNIT(*)
PLANE_ANGLE_UNIT()
SI_UNIT($,.RADIAN.)
);
#135286=(
NAMED_UNIT(*)
SI_UNIT($,.STERADIAN.)
SOLID_ANGLE_UNIT()
);
#135297=SHAPE_DEFINITION_REPRESENTATION(#135311,#135346);
#135311=PRODUCT_DEFINITION_SHAPE('',$,#135361);
#135346=SHAPE_REPRESENTATION('',(#33493),#135278);
#135350=PRODUCT_DEFINITION_CONTEXT('part definition',#135394,'design');
#135361=PRODUCT_DEFINITION('2026-10-15-19-09-11-259',
'Feed Screw End Block',#135375,#135350);
#135375=PRODUCT_DEFINITION_FORMATION('',$,#135406);
#135394=APPLICATION_CONTEXT(
'Core Data for Automotive Mechanical Design Process');
#135395=PRODUCT_CONTEXT('part definition',#135394,'mechanical');
#135406=PRODUCT('2026-10-15-19-09-11-259','Feed Screw End Block',$,(#135395));
#135420=PRESENTATION_STYLE_ASSIGNMENT((#135434));
#135434=SURFACE_STYLE_USAGE(.BOTH.,#135448);
#135448=SURFACE_SIDE_STYLE('',(#135462));
#135462=SURFACE_STYLE_FILL_AREA(#135476);
#135476=FILL_AREA_STYLE('Opaque(212,215,220)',(#135490));
#135490=FILL_AREA_STYLE_COLOUR('Opaque(212,215,220)',#135504);
#135504=COLOUR_RGB('Opaque(212,215,220)', 0.40784314, 0.44705882, 0.49803922);
ENDSEC;
END-ISO-10303-21;
